ISO-10303-21;
HEADER;
FILE_DESCRIPTION (('STEP AP214'),
    '1' );
FILE_NAME ('15. Rubber Handle Cover.step',
    '2026-10-09T14:04:53',
    ( '' ),
    ( '' ),
    'SwSTEP 2.0',
    'SolidWorks 2021',
    '' );
FILE_SCHEMA (( 'AUTOMOTIVE_DESIGN' ));
ENDSEC;

DATA;
#533=SHAPE_REPRESENTATION ( '15. Rubber Handle Cover', ( #10728 ), #93743 ) ;
#605=EDGE_CURVE ( 'NONE', #80946, #83274, #40402, .T. ) ;
#772=LINE ( 'NONE', #67688, #12340 ) ;
#779=ORIENTED_EDGE ( 'NONE', *, *, #7201, .F. ) ;
#808=DIRECTION ( 'NONE',  ( -1.000000000000000000, 0.000000000000000000, 0.000000000000000000 ) ) ;
#1014=DIRECTION ( 'NONE',  ( 3.469446951953614189E-16, -1.000000000000000000, 0.000000000000000000 ) ) ;
#1094=DIRECTION ( 'NONE',  ( -1.000000000000000000, 0.000000000000000000, 0.000000000000000000 ) ) ;
#1508=EDGE_LOOP ( 'NONE', ( #97538, #59106, #779, #30356 ) ) ;
#1606=ORIENTED_EDGE ( 'NONE', *, *, #52137, .F. ) ;
#2099=CARTESIAN_POINT ( 'NONE',  ( 19.00000000000001066, -4.000000000000000000, -1.500000000000000000 ) ) ;
#2103=PLANE ( 'NONE',  #91243 ) ;
#2138=VERTEX_POINT ( 'NONE', #37157 ) ;
#2222=VECTOR ( 'NONE', #11886, 1000.000000000000000 ) ;
#2380=ORIENTED_EDGE ( 'NONE', *, *, #101889, .T. ) ;
#2861=ORIENTED_EDGE ( 'NONE', *, *, #59032, .T. ) ;
#3016=ADVANCED_FACE ( 'NONE', ( #87556 ), #6612, .T. ) ;
#3069=FACE_OUTER_BOUND ( 'NONE', #14383, .T. ) ;
#3296=DIRECTION ( 'NONE',  ( -1.000000000000000000, -0.000000000000000000, 0.000000000000000000 ) ) ;
#3329=EDGE_CURVE ( 'NONE', #8093, #72947, #61975, .T. ) ;
#3583=ORIENTED_EDGE ( 'NONE', *, *, #83118, .T. ) ;
#3594=ORIENTED_EDGE ( 'NONE', *, *, #68800, .F. ) ;
#3668=ORIENTED_EDGE ( 'NONE', *, *, #81648, .T. ) ;
#3813=ORIENTED_EDGE ( 'NONE', *, *, #37842, .F. ) ;
#4262=SURFACE_STYLE_USAGE ( .BOTH. , #54366 ) ;
#4490=ORIENTED_EDGE ( 'NONE', *, *, #40700, .T. ) ;
#4810=FILL_AREA_STYLE ('',( #78159 ) ) ;
#4898=CARTESIAN_POINT ( 'NONE',  ( -19.99999999999999289, -5.000000000000000000, 25.00000000000000000 ) ) ;
#5084=ORIENTED_EDGE ( 'NONE', *, *, #65219, .T. ) ;
#5269=VECTOR ( 'NONE', #48043, 1000.000000000000000 ) ;
#6078=DIRECTION ( 'NONE',  ( -1.000000000000000000, -0.000000000000000000, -0.000000000000000000 ) ) ;
#6171=VERTEX_POINT ( 'NONE', #27415 ) ;
#6335=VERTEX_POINT ( 'NONE', #54798 ) ;
#6348=ORIENTED_EDGE ( 'NONE', *, *, #14083, .F. ) ;
#6364=AXIS2_PLACEMENT_3D ( 'NONE', #54817, #69442, #61352 ) ;
#6576=CARTESIAN_POINT ( 'NONE',  ( -18.99999999999999289, 5.000000000000000888, 25.00000000000000000 ) ) ;
#6612=CYLINDRICAL_SURFACE ( 'NONE', #29043, 1.000000000000000888 ) ;
#6729=DIRECTION ( 'NONE',  ( 0.000000000000000000, 0.000000000000000000, -1.000000000000000000 ) ) ;
#7201=EDGE_CURVE ( 'NONE', #47934, #88346, #51149, .T. ) ;
#7369=CARTESIAN_POINT ( 'NONE',  ( -19.99999999999999289, 5.000000000000000888, 25.00000000000000000 ) ) ;
#7556=VERTEX_POINT ( 'NONE', #43434 ) ;
#7604=DIRECTION ( 'NONE',  ( 0.000000000000000000, 1.000000000000000000, 0.000000000000000000 ) ) ;
#7642=MECHANICAL_DESIGN_GEOMETRIC_PRESENTATION_REPRESENTATION('',(#52453),#86909);
#7715=PLANE ( 'NONE',  #32536 ) ;
#7796=ADVANCED_FACE ( 'NONE', ( #8263 ), #33110, .T. ) ;
#7834=AXIS2_PLACEMENT_3D ( 'NONE', #55095, #96115, #64285 ) ;
#8093=VERTEX_POINT ( 'NONE', #15166 ) ;
#8231=ORIENTED_EDGE ( 'NONE', *, *, #88367, .F. ) ;
#8263=FACE_OUTER_BOUND ( 'NONE', #76176, .T. ) ;
#8465=ORIENTED_EDGE ( 'NONE', *, *, #19065, .T. ) ;
#8669=DIRECTION ( 'NONE',  ( -1.000000000000000000, 0.000000000000000000, 0.000000000000000000 ) ) ;
#8682=CARTESIAN_POINT ( 'NONE',  ( -18.99999999999999289, 4.000000000000000888, -1.500000000000001332 ) ) ;
#8783=VECTOR ( 'NONE', #104796, 1000.000000000000000 ) ;
#8790=AXIS2_PLACEMENT_3D ( 'NONE', #51226, #45299, #60435 ) ;
#9508=VECTOR ( 'NONE', #55206, 1000.000000000000000 ) ;
#9535=AXIS2_PLACEMENT_3D ( 'NONE', #19895, #12800, #45716 ) ;
#9667=DIRECTION ( 'NONE',  ( 0.000000000000000000, 1.000000000000000000, 0.000000000000000000 ) ) ;
#9704=AXIS2_PLACEMENT_3D ( 'NONE', #12770, #54821, #62413 ) ;
#9851=DIRECTION ( 'NONE',  ( -0.000000000000000000, 0.000000000000000000, 1.000000000000000000 ) ) ;
#10183=ORIENTED_EDGE ( 'NONE', *, *, #85721, .T. ) ;
#10395=CARTESIAN_POINT ( 'NONE',  ( -18.99999999999999289, -4.000000000000000000, 25.00000000000000000 ) ) ;
#10474=CARTESIAN_POINT ( 'NONE',  ( 19.00000000000000711, 5.000000000000000888, 25.00000000000000000 ) ) ;
#10617=CARTESIAN_POINT ( 'NONE',  ( 19.00000000000001066, -4.000000000000000000, -2.500000000000000000 ) ) ;
#10651=VERTEX_POINT ( 'NONE', #98290 ) ;
#10728=AXIS2_PLACEMENT_3D ( 'NONE', #14983, #57033, #47878 ) ;
#10790=CARTESIAN_POINT ( 'NONE',  ( -18.99999999999999289, -5.000000000000000000, -1.500000000000001332 ) ) ;
#11050=PRODUCT_DEFINITION_SHAPE ( 'NONE', 'NONE',  #25882 ) ;
#11170=EDGE_CURVE ( 'NONE', #68599, #10651, #102651, .T. ) ;
#11278=AXIS2_PLACEMENT_3D ( 'NONE', #2099, #101352, #100804 ) ;
#11292=EDGE_CURVE ( 'NONE', #53736, #36077, #20090, .T. ) ;
#11613=ORIENTED_EDGE ( 'NONE', *, *, #19066, .T. ) ;
#11623=ORIENTED_EDGE ( 'NONE', *, *, #29375, .T. ) ;
#11677=AXIS2_PLACEMENT_3D ( 'NONE', #90014, #106175, #32337 ) ;
#11886=DIRECTION ( 'NONE',  ( -0.000000000000000000, -0.000000000000000000, -1.000000000000000000 ) ) ;
#12340=VECTOR ( 'NONE', #26209, 1000.000000000000000 ) ;
#12770=CARTESIAN_POINT ( 'NONE',  ( -17.49999999999999645, -2.499999999999999556, 25.00000000000000000 ) ) ;
#12800=DIRECTION ( 'NONE',  ( 0.000000000000000000, -1.000000000000000000, 0.000000000000000000 ) ) ;
#13245=DIRECTION ( 'NONE',  ( -1.000000000000000000, 0.000000000000000000, -0.000000000000000000 ) ) ;
#13356=ADVANCED_FACE ( 'NONE', ( #3069 ), #44070, .T. ) ;
#13419=VECTOR ( 'NONE', #105664, 1000.000000000000000 ) ;
#13592=ORIENTED_EDGE ( 'NONE', *, *, #14083, .T. ) ;
#13958=LINE ( 'NONE', #97527, #80366 ) ;
#14083=EDGE_CURVE ( 'NONE', #48559, #88005, #23941, .T. ) ;
#14162=CIRCLE ( 'NONE', #48652, 1.000000000000000888 ) ;
#14199=CARTESIAN_POINT ( 'NONE',  ( 20.00000000000000711, 5.000000000000000888, 25.00000000000000000 ) ) ;
#14265=CARTESIAN_POINT ( 'NONE',  ( -17.49999999999999645, 2.500000000000000444, 25.00000000000000000 ) ) ;
#14383=EDGE_LOOP ( 'NONE', ( #93587, #102914, #47852, #29680 ) ) ;
#14925=EDGE_CURVE ( 'NONE', #85025, #8093, #13958, .T. ) ;
#14931=DIRECTION ( 'NONE',  ( 0.000000000000000000, -1.000000000000000000, 0.000000000000000000 ) ) ;
#14983=CARTESIAN_POINT ( 'NONE',  ( 0.000000000000000000, 0.000000000000000000, 0.000000000000000000 ) ) ;
#15166=CARTESIAN_POINT ( 'NONE',  ( -17.49999999999999645, -2.499999999999999556, 25.00000000000000000 ) ) ;
#15292=DIRECTION ( 'NONE',  ( 1.000000000000000000, 0.000000000000000000, 0.000000000000000000 ) ) ;
#15684=LINE ( 'NONE', #96622, #5269 ) ;
#16338=DIRECTION ( 'NONE',  ( -0.000000000000000000, -0.000000000000000000, 1.000000000000000000 ) ) ;
#16793=MANIFOLD_SOLID_BREP ( 'Fillet2', #94614 ) ;
#17268=DIRECTION ( 'NONE',  ( 0.000000000000000000, 0.000000000000000000, 1.000000000000000000 ) ) ;
#18238=DIRECTION ( 'NONE',  ( 1.000000000000000000, -0.000000000000000000, 0.000000000000000000 ) ) ;
#18418=EDGE_LOOP ( 'NONE', ( #40968, #101655, #11623, #96639 ) ) ;
#18526=FACE_OUTER_BOUND ( 'NONE', #73467, .T. ) ;
#19065=EDGE_CURVE ( 'NONE', #81772, #2138, #86284, .T. ) ;
#19066=EDGE_CURVE ( 'NONE', #10651, #36077, #95451, .T. ) ;
#19169=AXIS2_PLACEMENT_3D ( 'NONE', #26973, #9667, #17268 ) ;
#19174=ORIENTED_EDGE ( 'NONE', *, *, #101889, .F. ) ;
#19346=CARTESIAN_POINT ( 'NONE',  ( 19.00000000000000711, 4.000000000000000888, -1.500000000000001332 ) ) ;
#19491=DIRECTION ( 'NONE',  ( 0.000000000000000000, 0.000000000000000000, 1.000000000000000000 ) ) ;
#19515=ORIENTED_EDGE ( 'NONE', *, *, #53580, .T. ) ;
#19771=DIRECTION ( 'NONE',  ( 0.000000000000000000, 0.000000000000000000, -1.000000000000000000 ) ) ;
#19895=CARTESIAN_POINT ( 'NONE',  ( -19.99999999999999289, 5.000000000000000888, 25.00000000000000000 ) ) ;
#20090=CIRCLE ( 'NONE', #33846, 1.000000000000000888 ) ;
#20517=VECTOR ( 'NONE', #76708, 1000.000000000000000 ) ;
#21305=CARTESIAN_POINT ( 'NONE',  ( -19.99999999999999289, -4.000000000000000000, 25.00000000000000000 ) ) ;
#21921=ADVANCED_FACE ( 'NONE', ( #40816 ), #47834, .T. ) ;
#22074=SHAPE_REPRESENTATION_RELATIONSHIP ( 'NONE' , 'NONE' ,  #533, #64127 ) ;
#22362=CARTESIAN_POINT ( 'NONE',  ( 19.00000000000001421, -4.999999999999999112, 25.00000000000000000 ) ) ;
#22471=CARTESIAN_POINT ( 'NONE',  ( -18.99999999999999289, 5.000000000000000888, 25.00000000000000000 ) ) ;
#22616=AXIS2_PLACEMENT_3D ( 'NONE', #25014, #75109, #24500 ) ;
#22625=AXIS2_PLACEMENT_3D ( 'NONE', #52328, #101948, #19491 ) ;
#23204=CARTESIAN_POINT ( 'NONE',  ( 20.00000000000000711, 4.000000000000000000, -1.500000000000000000 ) ) ;
#23463=ORIENTED_EDGE ( 'NONE', *, *, #78011, .F. ) ;
#23475=ORIENTED_EDGE ( 'NONE', *, *, #14925, .T. ) ;
#23495=PLANE ( 'NONE',  #82916 ) ;
#23655=CIRCLE ( 'NONE', #6364, 1.000000000000000000 ) ;
#23665=DIRECTION ( 'NONE',  ( -1.000000000000000000, 0.000000000000000000, 0.000000000000000000 ) ) ;
#23806=VECTOR ( 'NONE', #96506, 1000.000000000000000 ) ;
#23941=LINE ( 'NONE', #14199, #25133 ) ;
#24097=DIRECTION ( 'NONE',  ( 0.000000000000000000, 0.000000000000000000, -1.000000000000000000 ) ) ;
#24280=AXIS2_PLACEMENT_3D ( 'NONE', #42020, #72782, #32897 ) ;
#24289=ORIENTED_EDGE ( 'NONE', *, *, #79603, .T. ) ;
#24328=DIRECTION ( 'NONE',  ( -1.000000000000000000, 0.000000000000000000, 0.000000000000000000 ) ) ;
#24500=DIRECTION ( 'NONE',  ( 0.000000000000000000, 1.000000000000000000, 0.000000000000000000 ) ) ;
#24562=ORIENTED_EDGE ( 'NONE', *, *, #71202, .T. ) ;
#24685=ORIENTED_EDGE ( 'NONE', *, *, #26050, .F. ) ;
#24736=CARTESIAN_POINT ( 'NONE',  ( 19.00000000000000711, 4.000000000000000000, -1.500000000000000000 ) ) ;
#25002=FACE_OUTER_BOUND ( 'NONE', #26825, .T. ) ;
#25014=CARTESIAN_POINT ( 'NONE',  ( 19.00000000000001066, -3.999999999999999112, -1.500000000000000000 ) ) ;
#25133=VECTOR ( 'NONE', #73494, 1000.000000000000000 ) ;
#25283=SPHERICAL_SURFACE ( 'NONE', #94413, 1.000000000000000000 ) ;
#25390=FACE_OUTER_BOUND ( 'NONE', #105657, .T. ) ;
#25620=ORIENTED_EDGE ( 'NONE', *, *, #605, .T. ) ;
#25882=PRODUCT_DEFINITION ( 'UNKNOWN', '', #48979, #93092 ) ;
#25940=AXIS2_PLACEMENT_3D ( 'NONE', #48324, #64537, #89866 ) ;
#25968=ORIENTED_EDGE ( 'NONE', *, *, #28672, .T. ) ;
#26050=EDGE_CURVE ( 'NONE', #53736, #68599, #105639, .T. ) ;
#26096=CARTESIAN_POINT ( 'NONE',  ( -18.99999999999999645, 4.000000000000000000, -2.500000000000000000 ) ) ;
#26146=LINE ( 'NONE', #39242, #30516 ) ;
#26209=DIRECTION ( 'NONE',  ( 1.000000000000000000, 0.000000000000000000, 0.000000000000000000 ) ) ;
#26576=COLOUR_RGB ( '', 0.31764706, 0.68627451, 0.89019608) ;
#26825=EDGE_LOOP ( 'NONE', ( #56411, #93207, #24562, #24289, #13592, #2861, #103757, #51228 ) ) ;
#26973=CARTESIAN_POINT ( 'NONE',  ( -18.99999999999999645, 4.000000000000000888, -1.500000000000000000 ) ) ;
#26991=EDGE_CURVE ( 'NONE', #53736, #53725, #72049, .T. ) ;
#27060=VECTOR ( 'NONE', #94866, 1000.000000000000000 ) ;
#27415=CARTESIAN_POINT ( 'NONE',  ( 17.50000000000000711, -2.499999999999999556, 0.000000000000000000 ) ) ;
#27484=PRODUCT ( '15. Rubber Handle Cover', '15. Rubber Handle Cover', '', ( #76028 ) ) ;
#27628=DIRECTION ( 'NONE',  ( 0.000000000000000000, -1.000000000000000000, 0.000000000000000000 ) ) ;
#28105=DIRECTION ( 'NONE',  ( 0.000000000000000000, 0.000000000000000000, -1.000000000000000000 ) ) ;
#28237=ADVANCED_FACE ( 'NONE', ( #53770 ), #45690, .T. ) ;
#28601=AXIS2_PLACEMENT_3D ( 'NONE', #10395, #93468, #44924 ) ;
#28672=EDGE_CURVE ( 'NONE', #47934, #7556, #68333, .T. ) ;
#29043=AXIS2_PLACEMENT_3D ( 'NONE', #38483, #88084, #47065 ) ;
#29244=EDGE_CURVE ( 'NONE', #6335, #47934, #88570, .T. ) ;
#29375=EDGE_CURVE ( 'NONE', #58207, #68198, #58872, .T. ) ;
#29680=ORIENTED_EDGE ( 'NONE', *, *, #68800, .T. ) ;
#29895=EDGE_LOOP ( 'NONE', ( #23463, #37123, #105013 ) ) ;
#30183=ORIENTED_EDGE ( 'NONE', *, *, #42972, .T. ) ;
#30245=DIRECTION ( 'NONE',  ( -1.000000000000000000, -2.168404344971008868E-17, 0.000000000000000000 ) ) ;
#30356=ORIENTED_EDGE ( 'NONE', *, *, #29244, .F. ) ;
#30500=ADVANCED_FACE ( 'NONE', ( #87418 ), #45885, .F. ) ;
#30516=VECTOR ( 'NONE', #105545, 1000.000000000000000 ) ;
#30540=ORIENTED_EDGE ( 'NONE', *, *, #31787, .F. ) ;
#30686=DIRECTION ( 'NONE',  ( -1.000000000000000000, 0.000000000000000000, 0.000000000000000000 ) ) ;
#30764=CARTESIAN_POINT ( 'NONE',  ( -17.49999999999999645, 2.500000000000000444, 25.00000000000000000 ) ) ;
#31093=ORIENTED_EDGE ( 'NONE', *, *, #65219, .F. ) ;
#31481=DIRECTION ( 'NONE',  ( 3.469446951953614189E-16, -1.000000000000000000, 0.000000000000000000 ) ) ;
#31653=CYLINDRICAL_SURFACE ( 'NONE', #25940, 1.000000000000000000 ) ;
#31694=DIRECTION ( 'NONE',  ( 0.000000000000000000, 0.000000000000000000, -1.000000000000000000 ) ) ;
#31787=EDGE_CURVE ( 'NONE', #68198, #80946, #46648, .T. ) ;
#31808=EDGE_LOOP ( 'NONE', ( #34228, #74633, #75974, #6348 ) ) ;
#32137=EDGE_LOOP ( 'NONE', ( #45288, #30540, #5084, #19515 ) ) ;
#32337=DIRECTION ( 'NONE',  ( 0.000000000000000000, 0.000000000000000000, -1.000000000000000000 ) ) ;
#32536=AXIS2_PLACEMENT_3D ( 'NONE', #57857, #106409, #15292 ) ;
#32592=ORIENTED_EDGE ( 'NONE', *, *, #59032, .F. ) ;
#32897=DIRECTION ( 'NONE',  ( 1.000000000000000000, 0.000000000000000000, 0.000000000000000000 ) ) ;
#33110=CYLINDRICAL_SURFACE ( 'NONE', #22616, 1.000000000000000000 ) ;
#33339=ADVANCED_FACE ( 'NONE', ( #68038 ), #68592, .T. ) ;
#33676=LINE ( 'NONE', #66548, #106659 ) ;
#33846=AXIS2_PLACEMENT_3D ( 'NONE', #96983, #73213, #30686 ) ;
#34066=VERTEX_POINT ( 'NONE', #74833 ) ;
#34228=ORIENTED_EDGE ( 'NONE', *, *, #52137, .T. ) ;
#34304=AXIS2_PLACEMENT_3D ( 'NONE', #101477, #27628, #35171 ) ;
#34336=EDGE_LOOP ( 'NONE', ( #25968, #68650, #8465, #88952 ) ) ;
#34604=DIRECTION ( 'NONE',  ( 0.000000000000000000, 0.000000000000000000, -1.000000000000000000 ) ) ;
#34969=CARTESIAN_POINT ( 'NONE',  ( 17.50000000000000711, -2.499999999999999556, 25.00000000000000000 ) ) ;
#35171=DIRECTION ( 'NONE',  ( 0.000000000000000000, 0.000000000000000000, -1.000000000000000000 ) ) ;
#35548=ADVANCED_FACE ( 'NONE', ( #18526 ), #51385, .T. ) ;
#35760=ADVANCED_FACE ( 'NONE', ( #97156 ), #105263, .F. ) ;
#35984=ADVANCED_FACE ( 'NONE', ( #42111 ), #81485, .T. ) ;
#36077=VERTEX_POINT ( 'NONE', #10790 ) ;
#36112=ORIENTED_EDGE ( 'NONE', *, *, #90251, .F. ) ;
#36138=DIRECTION ( 'NONE',  ( -0.000000000000000000, 0.000000000000000000, 1.000000000000000000 ) ) ;
#36156=( NAMED_UNIT ( * ) PLANE_ANGLE_UNIT ( ) SI_UNIT ( $, .RADIAN. ) );
#36929=ORIENTED_EDGE ( 'NONE', *, *, #64930, .F. ) ;
#37123=ORIENTED_EDGE ( 'NONE', *, *, #70933, .T. ) ;
#37157=CARTESIAN_POINT ( 'NONE',  ( 19.00000000000001421, -3.999999999999999112, -2.500000000000000000 ) ) ;
#37206=SURFACE_SIDE_STYLE ('',( #93822 ) ) ;
#37747=( NAMED_UNIT ( * ) SI_UNIT ( $, .STERADIAN. ) SOLID_ANGLE_UNIT ( ) );
#37842=EDGE_CURVE ( 'NONE', #2138, #53725, #26146, .T. ) ;
#38018=AXIS2_PLACEMENT_3D ( 'NONE', #38109, #79584, #13245 ) ;
#38109=CARTESIAN_POINT ( 'NONE',  ( 19.00000000000001066, -4.000000000000000000, 0.000000000000000000 ) ) ;
#38267=( LENGTH_UNIT ( ) NAMED_UNIT ( * ) SI_UNIT ( .MILLI., .METRE. ) );
#38429=ORIENTED_EDGE ( 'NONE', *, *, #81648, .F. ) ;
#38483=CARTESIAN_POINT ( 'NONE',  ( 19.00000000000001066, -4.000000000000000000, 25.00000000000000000 ) ) ;
#38532=LINE ( 'NONE', #22362, #9508 ) ;
#38710=LINE ( 'NONE', #7369, #77896 ) ;
#39107=DIRECTION ( 'NONE',  ( 0.000000000000000000, -1.000000000000000000, 0.000000000000000000 ) ) ;
#39242=CARTESIAN_POINT ( 'NONE',  ( -18.99999999999999645, -4.000000000000000000, -2.500000000000000000 ) ) ;
#39310=CARTESIAN_POINT ( 'NONE',  ( -18.99999999999999289, 4.000000000000000888, -1.500000000000001332 ) ) ;
#39510=ADVANCED_FACE ( 'NONE', ( #25390 ), #88660, .T. ) ;
#39559=CARTESIAN_POINT ( 'NONE',  ( 19.00000000000001066, -4.000000000000000000, -2.500000000000000000 ) ) ;
#39662=EDGE_LOOP ( 'NONE', ( #36112, #3583, #72482, #106251 ) ) ;
#39726=ORIENTED_EDGE ( 'NONE', *, *, #106755, .F. ) ;
#39731=FACE_OUTER_BOUND ( 'NONE', #29895, .T. ) ;
#39847=ORIENTED_EDGE ( 'NONE', *, *, #82682, .T. ) ;
#40068=ORIENTED_EDGE ( 'NONE', *, *, #3329, .F. ) ;
#40244=FACE_OUTER_BOUND ( 'NONE', #1508, .T. ) ;
#40283=UNCERTAINTY_MEASURE_WITH_UNIT (LENGTH_MEASURE( 1.000000000000000082E-05 ), #53360, 'distance_accuracy_value', 'NONE');
#40402=LINE ( 'NONE', #72757, #13419 ) ;
#40540=DIRECTION ( 'NONE',  ( -0.000000000000000000, 1.000000000000000000, -0.000000000000000000 ) ) ;
#40593=DIRECTION ( 'NONE',  ( -1.000000000000000000, 0.000000000000000000, 0.000000000000000000 ) ) ;
#40700=EDGE_CURVE ( 'NONE', #58207, #6171, #63617, .T. ) ;
#40702=FACE_OUTER_BOUND ( 'NONE', #79016, .T. ) ;
#40816=FACE_OUTER_BOUND ( 'NONE', #39662, .T. ) ;
#40903=ORIENTED_EDGE ( 'NONE', *, *, #14925, .F. ) ;
#40968=ORIENTED_EDGE ( 'NONE', *, *, #69857, .F. ) ;
#40985=ORIENTED_EDGE ( 'NONE', *, *, #69857, .T. ) ;
#41054=ORIENTED_EDGE ( 'NONE', *, *, #11292, .F. ) ;
#41231=ORIENTED_EDGE ( 'NONE', *, *, #70933, .F. ) ;
#42020=CARTESIAN_POINT ( 'NONE',  ( -18.99999999999999289, 4.000000000000000888, 25.00000000000000000 ) ) ;
#42098=CARTESIAN_POINT ( 'NONE',  ( 17.50000000000000711, 2.500000000000000444, 25.00000000000000000 ) ) ;
#42111=FACE_OUTER_BOUND ( 'NONE', #88215, .T. ) ;
#42196=CARTESIAN_POINT ( 'NONE',  ( 19.00000000000001421, -4.999999999999999112, -1.500000000000000000 ) ) ;
#42404=UNCERTAINTY_MEASURE_WITH_UNIT (LENGTH_MEASURE( 1.000000000000000082E-05 ), #38267, 'distance_accuracy_value', 'NONE');
#42576=FACE_OUTER_BOUND ( 'NONE', #31808, .T. ) ;
#42580=CARTESIAN_POINT ( 'NONE',  ( -17.49999999999999645, 2.500000000000000444, 0.000000000000000000 ) ) ;
#42972=EDGE_CURVE ( 'NONE', #88975, #53736, #73092, .T. ) ;
#43113=FACE_OUTER_BOUND ( 'NONE', #34336, .T. ) ;
#43434=CARTESIAN_POINT ( 'NONE',  ( 20.00000000000000711, 4.000000000000000888, -1.500000000000001332 ) ) ;
#43456=ADVANCED_FACE ( 'NONE', ( #25002, #89192 ), #7715, .T. ) ;
#43498=ORIENTED_EDGE ( 'NONE', *, *, #82682, .F. ) ;
#43706=ORIENTED_EDGE ( 'NONE', *, *, #78011, .T. ) ;
#43826=CARTESIAN_POINT ( 'NONE',  ( 19.00000000000001421, -4.999999999999999112, 25.00000000000000000 ) ) ;
#43907=CARTESIAN_POINT ( 'NONE',  ( 17.50000000000000711, 2.500000000000000444, 0.000000000000000000 ) ) ;
#44070=PLANE ( 'NONE',  #78302 ) ;
#44377=ADVANCED_FACE ( 'NONE', ( #74844 ), #25283, .T. ) ;
#44562=ORIENTED_EDGE ( 'NONE', *, *, #29375, .F. ) ;
#44723=ORIENTED_EDGE ( 'NONE', *, *, #79195, .F. ) ;
#44740=EDGE_LOOP ( 'NONE', ( #105725, #19174, #55957 ) ) ;
#44745=ADVANCED_FACE ( 'NONE', ( #98727 ), #82565, .T. ) ;
#44814=LINE ( 'NONE', #30764, #2222 ) ;
#44871=AXIS2_PLACEMENT_3D ( 'NONE', #91499, #50473, #83384 ) ;
#44899=DIRECTION ( 'NONE',  ( -1.000000000000000000, -0.000000000000000000, -0.000000000000000000 ) ) ;
#44924=DIRECTION ( 'NONE',  ( -1.000000000000000000, 0.000000000000000000, 0.000000000000000000 ) ) ;
#45263=PRESENTATION_STYLE_ASSIGNMENT (( #4262 ) ) ;
#45280=SHAPE_DEFINITION_REPRESENTATION ( #11050, #533 ) ;
#45288=ORIENTED_EDGE ( 'NONE', *, *, #605, .F. ) ;
#45299=DIRECTION ( 'NONE',  ( -0.000000000000000000, 0.000000000000000000, 1.000000000000000000 ) ) ;
#45690=PLANE ( 'NONE',  #9704 ) ;
#45716=DIRECTION ( 'NONE',  ( 0.000000000000000000, -0.000000000000000000, -1.000000000000000000 ) ) ;
#45880=ORIENTED_EDGE ( 'NONE', *, *, #81625, .F. ) ;
#45885=PLANE ( 'NONE',  #65149 ) ;
#46648=LINE ( 'NONE', #62857, #89423 ) ;
#46772=PLANE ( 'NONE',  #9535 ) ;
#46879=CARTESIAN_POINT ( 'NONE',  ( 20.00000000000000711, 4.000000000000000888, 25.00000000000000000 ) ) ;
#47065=DIRECTION ( 'NONE',  ( -1.000000000000000000, 0.000000000000000000, 0.000000000000000000 ) ) ;
#47123=EDGE_CURVE ( 'NONE', #92851, #74216, #86331, .T. ) ;
#47228=( GEOMETRIC_REPRESENTATION_CONTEXT ( 3 ) GLOBAL_UNCERTAINTY_ASSIGNED_CONTEXT ( ( #42404 ) ) GLOBAL_UNIT_ASSIGNED_CONTEXT ( ( #38267, #90364, #57444 ) ) REPRESENTATION_CONTEXT ( 'NONE', 'WORKASPACE' ) );
#47694=DIRECTION ( 'NONE',  ( 0.000000000000000000, -0.000000000000000000, -1.000000000000000000 ) ) ;
#47834=CYLINDRICAL_SURFACE ( 'NONE', #68058, 1.000000000000000888 ) ;
#47852=ORIENTED_EDGE ( 'NONE', *, *, #37842, .T. ) ;
#47878=DIRECTION ( 'NONE',  ( 1.000000000000000000, 0.000000000000000000, 0.000000000000000000 ) ) ;
#47934=VERTEX_POINT ( 'NONE', #95774 ) ;
#47979=DIRECTION ( 'NONE',  ( -2.168404344971008868E-17, 1.000000000000000000, 0.000000000000000000 ) ) ;
#47980=ADVANCED_FACE ( 'NONE', ( #40702 ), #23495, .T. ) ;
#48043=DIRECTION ( 'NONE',  ( -0.000000000000000000, -0.000000000000000000, 1.000000000000000000 ) ) ;
#48144=LINE ( 'NONE', #39559, #78713 ) ;
#48234=CARTESIAN_POINT ( 'NONE',  ( -18.99999999999999289, 4.000000000000000888, -1.500000000000000444 ) ) ;
#48324=CARTESIAN_POINT ( 'NONE',  ( 19.00000000000001066, 4.000000000000000000, -1.500000000000000000 ) ) ;
#48559=VERTEX_POINT ( 'NONE', #102411 ) ;
#48652=AXIS2_PLACEMENT_3D ( 'NONE', #39310, #105609, #23665 ) ;
#48856=DIRECTION ( 'NONE',  ( -0.000000000000000000, 1.000000000000000000, -0.000000000000000000 ) ) ;
#48894=DIRECTION ( 'NONE',  ( -1.000000000000000000, 0.000000000000000000, 0.000000000000000000 ) ) ;
#48979=PRODUCT_DEFINITION_FORMATION_WITH_SPECIFIED_SOURCE ( 'ANY', '', #27484, .NOT_KNOWN. ) ;
#49042=EDGE_LOOP ( 'NONE', ( #88749, #40985, #25620, #3668 ) ) ;
#49198=LINE ( 'NONE', #82098, #8783 ) ;
#49224=DIRECTION ( 'NONE',  ( -1.000000000000000000, 0.000000000000000000, 0.000000000000000000 ) ) ;
#49291=CARTESIAN_POINT ( 'NONE',  ( 19.00000000000000711, 5.000000000000000888, -1.500000000000001332 ) ) ;
#49489=CIRCLE ( 'NONE', #52964, 1.000000000000000888 ) ;
#49584=EDGE_CURVE ( 'NONE', #50075, #92851, #60633, .T. ) ;
#49925=DIRECTION ( 'NONE',  ( 0.000000000000000000, 1.000000000000000000, 0.000000000000000000 ) ) ;
#50075=VERTEX_POINT ( 'NONE', #85037 ) ;
#50473=DIRECTION ( 'NONE',  ( 1.000000000000000000, 0.000000000000000000, 0.000000000000000000 ) ) ;
#51094=DIRECTION ( 'NONE',  ( 0.000000000000000000, 0.000000000000000000, -1.000000000000000000 ) ) ;
#51149=CIRCLE ( 'NONE', #82182, 1.000000000000000000 ) ;
#51226=CARTESIAN_POINT ( 'NONE',  ( 19.00000000000001066, -4.000000000000000000, 25.00000000000000000 ) ) ;
#51228=ORIENTED_EDGE ( 'NONE', *, *, #47123, .T. ) ;
#51385=CYLINDRICAL_SURFACE ( 'NONE', #28601, 1.000000000000000888 ) ;
#51455=EDGE_LOOP ( 'NONE', ( #89120, #40068, #100344, #4490 ) ) ;
#51620=VECTOR ( 'NONE', #48856, 1000.000000000000000 ) ;
#52137=EDGE_CURVE ( 'NONE', #48559, #81772, #66646, .T. ) ;
#52328=CARTESIAN_POINT ( 'NONE',  ( 19.00000000000001066, -4.000000000000000000, -1.500000000000001332 ) ) ;
#52453=STYLED_ITEM ( 'NONE', ( #45263 ), #16793 ) ;
#52789=APPLICATION_CONTEXT ( 'automotive_design' ) ;
#52964=AXIS2_PLACEMENT_3D ( 'NONE', #98855, #9851, #83220 ) ;
#53076=ORIENTED_EDGE ( 'NONE', *, *, #71202, .F. ) ;
#53264=ORIENTED_EDGE ( 'NONE', *, *, #87288, .T. ) ;
#53360=( LENGTH_UNIT ( ) NAMED_UNIT ( * ) SI_UNIT ( .MILLI., .METRE. ) );
#53580=EDGE_CURVE ( 'NONE', #85025, #83274, #44814, .T. ) ;
#53725=VERTEX_POINT ( 'NONE', #73290 ) ;
#53736=VERTEX_POINT ( 'NONE', #57112 ) ;
#53745=DIRECTION ( 'NONE',  ( -1.000000000000000000, 0.000000000000000000, -0.000000000000000000 ) ) ;
#53770=FACE_OUTER_BOUND ( 'NONE', #51455, .T. ) ;
#53919=CARTESIAN_POINT ( 'NONE',  ( -18.99999999999999289, -5.000000000000000000, 25.00000000000000000 ) ) ;
#54366=SURFACE_SIDE_STYLE ('',( #99759 ) ) ;
#54764=CARTESIAN_POINT ( 'NONE',  ( -19.99999999999999289, 4.000000000000000888, -1.500000000000001332 ) ) ;
#54798=CARTESIAN_POINT ( 'NONE',  ( -18.99999999999999645, 4.000000000000000888, -2.500000000000000000 ) ) ;
#54817=CARTESIAN_POINT ( 'NONE',  ( -18.99999999999999289, -4.000000000000000000, -1.500000000000001332 ) ) ;
#54821=DIRECTION ( 'NONE',  ( 0.000000000000000000, 1.000000000000000000, 0.000000000000000000 ) ) ;
#55095=CARTESIAN_POINT ( 'NONE',  ( -19.99999999999999289, 5.000000000000000888, 25.00000000000000000 ) ) ;
#55206=DIRECTION ( 'NONE',  ( -0.000000000000000000, -0.000000000000000000, 1.000000000000000000 ) ) ;
#55397=CARTESIAN_POINT ( 'NONE',  ( -18.99999999999999289, 4.000000000000000888, 25.00000000000000000 ) ) ;
#55490=ORIENTED_EDGE ( 'NONE', *, *, #58352, .F. ) ;
#55827=DIRECTION ( 'NONE',  ( -0.000000000000000000, -0.000000000000000000, 1.000000000000000000 ) ) ;
#55957=ORIENTED_EDGE ( 'NONE', *, *, #28672, .F. ) ;
#56284=EDGE_LOOP ( 'NONE', ( #11613, #39847, #82985, #53076 ) ) ;
#56411=ORIENTED_EDGE ( 'NONE', *, *, #106755, .T. ) ;
#56536=DIRECTION ( 'NONE',  ( 0.000000000000000000, -1.000000000000000000, 0.000000000000000000 ) ) ;
#56752=CIRCLE ( 'NONE', #60275, 1.000000000000000888 ) ;
#56842=ADVANCED_FACE ( 'NONE', ( #86727 ), #46772, .F. ) ;
#56942=SPHERICAL_SURFACE ( 'NONE', #91343, 1.000000000000000000 ) ;
#57014=AXIS2_PLACEMENT_3D ( 'NONE', #14265, #39107, #47694 ) ;
#57033=DIRECTION ( 'NONE',  ( 0.000000000000000000, 0.000000000000000000, 1.000000000000000000 ) ) ;
#57112=CARTESIAN_POINT ( 'NONE',  ( -19.99999999999999289, -4.000000000000000000, -1.500000000000001332 ) ) ;
#57289=DIRECTION ( 'NONE',  ( -0.000000000000000000, -0.000000000000000000, 1.000000000000000000 ) ) ;
#57416=ORIENTED_EDGE ( 'NONE', *, *, #90251, .T. ) ;
#57438=CARTESIAN_POINT ( 'NONE',  ( -19.99999999999999289, 4.000000000000000888, 25.00000000000000000 ) ) ;
#57444=( NAMED_UNIT ( * ) SI_UNIT ( $, .STERADIAN. ) SOLID_ANGLE_UNIT ( ) );
#57478=CARTESIAN_POINT ( 'NONE',  ( 17.50000000000000711, 2.500000000000000444, 0.000000000000000000 ) ) ;
#57857=CARTESIAN_POINT ( 'NONE',  ( 0.000000000000000000, 0.000000000000000000, 25.00000000000000000 ) ) ;
#58207=VERTEX_POINT ( 'NONE', #34969 ) ;
#58285=DIRECTION ( 'NONE',  ( 0.000000000000000000, 0.000000000000000000, 1.000000000000000000 ) ) ;
#58352=EDGE_CURVE ( 'NONE', #36077, #53725, #23655, .T. ) ;
#58463=DIRECTION ( 'NONE',  ( 1.000000000000000000, 2.168404344971008560E-17, 0.000000000000000000 ) ) ;
#58693=DIRECTION ( 'NONE',  ( 0.000000000000000000, 1.000000000000000000, 0.000000000000000000 ) ) ;
#58783=CIRCLE ( 'NONE', #8790, 1.000000000000000888 ) ;
#58872=LINE ( 'NONE', #83129, #102888 ) ;
#59032=EDGE_CURVE ( 'NONE', #88005, #50075, #49489, .T. ) ;
#59106=ORIENTED_EDGE ( 'NONE', *, *, #85721, .F. ) ;
#59387=EDGE_LOOP ( 'NONE', ( #68045, #30183, #72005, #39726 ) ) ;
#59389=FACE_OUTER_BOUND ( 'NONE', #73988, .T. ) ;
#59784=AXIS2_PLACEMENT_3D ( 'NONE', #76881, #68819, #19771 ) ;
#59852=DIRECTION ( 'NONE',  ( -1.000000000000000000, -3.469446951953614189E-16, 0.000000000000000000 ) ) ;
#59857=DIRECTION ( 'NONE',  ( 0.000000000000000000, -1.000000000000000000, 0.000000000000000000 ) ) ;
#59878=CARTESIAN_POINT ( 'NONE',  ( 17.50000000000000711, 2.500000000000000444, 25.00000000000000000 ) ) ;
#60275=AXIS2_PLACEMENT_3D ( 'NONE', #91311, #16338, #49224 ) ;
#60435=DIRECTION ( 'NONE',  ( 1.000000000000000000, 0.000000000000000000, 0.000000000000000000 ) ) ;
#60633=LINE ( 'NONE', #85420, #89645 ) ;
#60658=DIRECTION ( 'NONE',  ( 0.000000000000000000, 0.000000000000000000, -1.000000000000000000 ) ) ;
#60729=EDGE_LOOP ( 'NONE', ( #31093, #44562, #90764, #40903 ) ) ;
#60914=CARTESIAN_POINT ( 'NONE',  ( -18.99999999999999289, -4.000000000000000000, 25.00000000000000000 ) ) ;
#61309=CIRCLE ( 'NONE', #83670, 1.000000000000000000 ) ;
#61352=DIRECTION ( 'NONE',  ( 0.000000000000000000, 0.000000000000000000, -1.000000000000000000 ) ) ;
#61449=CARTESIAN_POINT ( 'NONE',  ( 20.00000000000001066, -4.000000000000000000, -1.500000000000001332 ) ) ;
#61975=LINE ( 'NONE', #76658, #27060 ) ;
#62326=DIRECTION ( 'NONE',  ( -0.000000000000000000, -0.000000000000000000, -1.000000000000000000 ) ) ;
#62413=DIRECTION ( 'NONE',  ( 0.000000000000000000, -0.000000000000000000, 1.000000000000000000 ) ) ;
#62857=CARTESIAN_POINT ( 'NONE',  ( 17.50000000000000711, 2.500000000000000444, 25.00000000000000000 ) ) ;
#63050=CARTESIAN_POINT ( 'NONE',  ( 19.00000000000001421, -4.999999999999999112, -1.500000000000001332 ) ) ;
#63172=VECTOR ( 'NONE', #97174, 1000.000000000000000 ) ;
#63507=ADVANCED_FACE ( 'NONE', ( #43113 ), #67917, .T. ) ;
#63617=LINE ( 'NONE', #78699, #23806 ) ;
#64127=ADVANCED_BREP_SHAPE_REPRESENTATION ( '', ( #16793, #10728 ), #93743 ) ;
#64285=DIRECTION ( 'NONE',  ( -0.000000000000000000, 0.000000000000000000, -1.000000000000000000 ) ) ;
#64304=CARTESIAN_POINT ( 'NONE',  ( 19.00000000000000711, 4.000000000000000000, -2.500000000000000000 ) ) ;
#64537=DIRECTION ( 'NONE',  ( -1.000000000000000000, 0.000000000000000000, 0.000000000000000000 ) ) ;
#64929=ORIENTED_EDGE ( 'NONE', *, *, #11170, .F. ) ;
#64930=EDGE_CURVE ( 'NONE', #68266, #104924, #38532, .T. ) ;
#65051=CARTESIAN_POINT ( 'NONE',  ( 20.00000000000001066, -4.000000000000000000, 25.00000000000000000 ) ) ;
#65149=AXIS2_PLACEMENT_3D ( 'NONE', #4898, #47979, #30245 ) ;
#65190=CARTESIAN_POINT ( 'NONE',  ( -19.99999999999999289, -4.000000000000000000, 25.00000000000000000 ) ) ;
#65219=EDGE_CURVE ( 'NONE', #68198, #85025, #93971, .T. ) ;
#65502=DIRECTION ( 'NONE',  ( 1.000000000000000000, 0.000000000000000000, 0.000000000000000000 ) ) ;
#65609=CIRCLE ( 'NONE', #19169, 1.000000000000000000 ) ;
#65626=VECTOR ( 'NONE', #28105, 1000.000000000000000 ) ;
#65763=DIRECTION ( 'NONE',  ( -3.469446951953614189E-16, 1.000000000000000000, -0.000000000000000000 ) ) ;
#65988=VECTOR ( 'NONE', #24097, 1000.000000000000000 ) ;
#66485=DIRECTION ( 'NONE',  ( 1.000000000000000000, 0.000000000000000000, 0.000000000000000000 ) ) ;
#66548=CARTESIAN_POINT ( 'NONE',  ( -19.99999999999999289, -5.000000000000000000, 25.00000000000000000 ) ) ;
#66646=LINE ( 'NONE', #65051, #65988 ) ;
#66873=FILL_AREA_STYLE ('',( #74937 ) ) ;
#66910=EDGE_CURVE ( 'NONE', #47934, #2138, #48144, .T. ) ;
#66915=AXIS2_PLACEMENT_3D ( 'NONE', #42098, #8669, #58285 ) ;
#67688=CARTESIAN_POINT ( 'NONE',  ( -17.49999999999999645, -2.499999999999999556, 25.00000000000000000 ) ) ;
#67917=CYLINDRICAL_SURFACE ( 'NONE', #11278, 1.000000000000000888 ) ;
#67997=CARTESIAN_POINT ( 'NONE',  ( 19.00000000000000711, 4.000000000000000888, 25.00000000000000000 ) ) ;
#68025=CARTESIAN_POINT ( 'NONE',  ( -18.99999999999999645, 5.000000000000000888, -1.500000000000000000 ) ) ;
#68038=FACE_OUTER_BOUND ( 'NONE', #68900, .T. ) ;
#68045=ORIENTED_EDGE ( 'NONE', *, *, #81129, .T. ) ;
#68058=AXIS2_PLACEMENT_3D ( 'NONE', #55397, #31694, #48894 ) ;
#68086=CARTESIAN_POINT ( 'NONE',  ( -17.49999999999999645, -2.499999999999999556, 0.000000000000000000 ) ) ;
#68198=VERTEX_POINT ( 'NONE', #59878 ) ;
#68266=VERTEX_POINT ( 'NONE', #63050 ) ;
#68333=CIRCLE ( 'NONE', #59784, 1.000000000000000000 ) ;
#68347=DIRECTION ( 'NONE',  ( 0.000000000000000000, 0.000000000000000000, -1.000000000000000000 ) ) ;
#68592=CYLINDRICAL_SURFACE ( 'NONE', #34304, 1.000000000000000000 ) ;
#68599=VERTEX_POINT ( 'NONE', #21305 ) ;
#68617=CARTESIAN_POINT ( 'NONE',  ( -17.49999999999999645, -2.499999999999999556, 0.000000000000000000 ) ) ;
#68650=ORIENTED_EDGE ( 'NONE', *, *, #93351, .F. ) ;
#68800=EDGE_CURVE ( 'NONE', #53725, #6335, #84279, .T. ) ;
#68819=DIRECTION ( 'NONE',  ( 0.000000000000000000, -1.000000000000000000, 0.000000000000000000 ) ) ;
#68900=EDGE_LOOP ( 'NONE', ( #101374, #95328, #45880, #3594 ) ) ;
#69442=DIRECTION ( 'NONE',  ( 1.000000000000000000, 0.000000000000000000, 0.000000000000000000 ) ) ;
#69529=ORIENTED_EDGE ( 'NONE', *, *, #83118, .F. ) ;
#69857=EDGE_CURVE ( 'NONE', #6171, #80946, #98998, .T. ) ;
#70075=SURFACE_STYLE_USAGE ( .BOTH. , #37206 ) ;
#70513=VECTOR ( 'NONE', #55827, 1000.000000000000000 ) ;
#70933=EDGE_CURVE ( 'NONE', #68266, #2138, #77578, .T. ) ;
#70967=VECTOR ( 'NONE', #65763, 1000.000000000000000 ) ;
#71202=EDGE_CURVE ( 'NONE', #10651, #104924, #33676, .T. ) ;
#72005=ORIENTED_EDGE ( 'NONE', *, *, #26050, .T. ) ;
#72049=CIRCLE ( 'NONE', #11677, 1.000000000000000000 ) ;
#72144=ORIENTED_EDGE ( 'NONE', *, *, #49584, .F. ) ;
#72482=ORIENTED_EDGE ( 'NONE', *, *, #81129, .F. ) ;
#72539=VECTOR ( 'NONE', #59857, 1000.000000000000000 ) ;
#72757=CARTESIAN_POINT ( 'NONE',  ( -17.49999999999999645, 2.500000000000000444, 0.000000000000000000 ) ) ;
#72782=DIRECTION ( 'NONE',  ( -0.000000000000000000, 0.000000000000000000, 1.000000000000000000 ) ) ;
#72947=VERTEX_POINT ( 'NONE', #68617 ) ;
#73092=LINE ( 'NONE', #81719, #82393 ) ;
#73213=DIRECTION ( 'NONE',  ( -0.000000000000000000, -0.000000000000000000, 1.000000000000000000 ) ) ;
#73290=CARTESIAN_POINT ( 'NONE',  ( -18.99999999999999289, -4.000000000000000000, -2.500000000000000000 ) ) ;
#73467=EDGE_LOOP ( 'NONE', ( #24685, #85364, #106088, #64929 ) ) ;
#73494=DIRECTION ( 'NONE',  ( -3.469446951953614189E-16, 1.000000000000000000, -0.000000000000000000 ) ) ;
#73988=EDGE_LOOP ( 'NONE', ( #44723, #2380, #103185, #32592 ) ) ;
#74124=CARTESIAN_POINT ( 'NONE',  ( -17.49999999999999645, 2.500000000000000444, 25.00000000000000000 ) ) ;
#74216=VERTEX_POINT ( 'NONE', #57438 ) ;
#74259=EDGE_CURVE ( 'NONE', #8093, #58207, #772, .T. ) ;
#74633=ORIENTED_EDGE ( 'NONE', *, *, #93351, .T. ) ;
#74703=MECHANICAL_DESIGN_GEOMETRIC_PRESENTATION_REPRESENTATION('',(#104041),#47228);
#74833=CARTESIAN_POINT ( 'NONE',  ( -18.99999999999999289, 5.000000000000000888, -1.500000000000001332 ) ) ;
#74844=FACE_OUTER_BOUND ( 'NONE', #44740, .T. ) ;
#74936=LINE ( 'NONE', #42580, #72539 ) ;
#74937=FILL_AREA_STYLE_COLOUR ( '', #97194 ) ;
#75079=DIRECTION ( 'NONE',  ( 1.000000000000000000, 2.168404344971008868E-17, -0.000000000000000000 ) ) ;
#75109=DIRECTION ( 'NONE',  ( 1.000000000000000000, 2.168404344971008868E-17, 0.000000000000000000 ) ) ;
#75388=DIRECTION ( 'NONE',  ( -1.000000000000000000, 0.000000000000000000, 0.000000000000000000 ) ) ;
#75974=ORIENTED_EDGE ( 'NONE', *, *, #79195, .T. ) ;
#76028=PRODUCT_CONTEXT ( 'NONE', #89957, 'mechanical' ) ;
#76107=UNCERTAINTY_MEASURE_WITH_UNIT (LENGTH_MEASURE( 1.000000000000000082E-05 ), #79735, 'distance_accuracy_value', 'NONE');
#76176=EDGE_LOOP ( 'NONE', ( #100280, #3813, #41231, #43498 ) ) ;
#76658=CARTESIAN_POINT ( 'NONE',  ( -17.49999999999999645, -2.499999999999999556, 25.00000000000000000 ) ) ;
#76708=DIRECTION ( 'NONE',  ( -0.000000000000000000, 1.000000000000000000, 0.000000000000000000 ) ) ;
#76881=CARTESIAN_POINT ( 'NONE',  ( 19.00000000000000711, 4.000000000000000888, -1.500000000000000444 ) ) ;
#77078=DIRECTION ( 'NONE',  ( 1.000000000000000000, 0.000000000000000000, 0.000000000000000000 ) ) ;
#77578=CIRCLE ( 'NONE', #44871, 1.000000000000000000 ) ;
#77621=( NAMED_UNIT ( * ) SI_UNIT ( $, .STERADIAN. ) SOLID_ANGLE_UNIT ( ) );
#77896=VECTOR ( 'NONE', #14931, 1000.000000000000000 ) ;
#78011=EDGE_CURVE ( 'NONE', #68266, #81772, #56752, .T. ) ;
#78159=FILL_AREA_STYLE_COLOUR ( '', #26576 ) ;
#78302=AXIS2_PLACEMENT_3D ( 'NONE', #10617, #68347, #53745 ) ;
#78699=CARTESIAN_POINT ( 'NONE',  ( 17.50000000000000711, -2.499999999999999556, 25.00000000000000000 ) ) ;
#78713=VECTOR ( 'NONE', #31481, 1000.000000000000000 ) ;
#78778=AXIS2_PLACEMENT_3D ( 'NONE', #81553, #57289, #40593 ) ;
#79016=EDGE_LOOP ( 'NONE', ( #38429, #99897, #23475, #82980 ) ) ;
#79195=EDGE_CURVE ( 'NONE', #7556, #88005, #15684, .T. ) ;
#79205=( NAMED_UNIT ( * ) PLANE_ANGLE_UNIT ( ) SI_UNIT ( $, .RADIAN. ) );
#79285=ORIENTED_EDGE ( 'NONE', *, *, #79603, .F. ) ;
#79584=DIRECTION ( 'NONE',  ( 0.000000000000000000, 0.000000000000000000, -1.000000000000000000 ) ) ;
#79603=EDGE_CURVE ( 'NONE', #104924, #48559, #58783, .T. ) ;
#79735=( LENGTH_UNIT ( ) NAMED_UNIT ( * ) SI_UNIT ( .MILLI., .METRE. ) );
#80143=ADVANCED_FACE ( 'NONE', ( #39731 ), #56942, .T. ) ;
#80222=ADVANCED_FACE ( 'NONE', ( #40244 ), #31653, .T. ) ;
#80366=VECTOR ( 'NONE', #56536, 1000.000000000000000 ) ;
#80589=ADVANCED_FACE ( 'NONE', ( #94737 ), #103856, .F. ) ;
#80946=VERTEX_POINT ( 'NONE', #43907 ) ;
#81129=EDGE_CURVE ( 'NONE', #74216, #88975, #49198, .T. ) ;
#81485=SPHERICAL_SURFACE ( 'NONE', #94008, 1.000000000000000000 ) ;
#81553=CARTESIAN_POINT ( 'NONE',  ( 19.00000000000000711, 4.000000000000000888, -1.500000000000001332 ) ) ;
#81625=EDGE_CURVE ( 'NONE', #6335, #88975, #65609, .T. ) ;
#81648=EDGE_CURVE ( 'NONE', #83274, #72947, #74936, .T. ) ;
#81719=CARTESIAN_POINT ( 'NONE',  ( -19.99999999999999289, -4.000000000000000000, -1.500000000000000000 ) ) ;
#81772=VERTEX_POINT ( 'NONE', #61449 ) ;
#82098=CARTESIAN_POINT ( 'NONE',  ( -19.99999999999999289, 4.000000000000000888, 25.00000000000000000 ) ) ;
#82182=AXIS2_PLACEMENT_3D ( 'NONE', #24736, #18238, #51094 ) ;
#82222=DIRECTION ( 'NONE',  ( -0.000000000000000000, 0.000000000000000000, -1.000000000000000000 ) ) ;
#82393=VECTOR ( 'NONE', #83335, 1000.000000000000000 ) ;
#82565=PLANE ( 'NONE',  #66915 ) ;
#82682=EDGE_CURVE ( 'NONE', #36077, #68266, #99901, .T. ) ;
#82916=AXIS2_PLACEMENT_3D ( 'NONE', #74124, #89273, #82222 ) ;
#82980=ORIENTED_EDGE ( 'NONE', *, *, #3329, .T. ) ;
#82985=ORIENTED_EDGE ( 'NONE', *, *, #64930, .T. ) ;
#83118=EDGE_CURVE ( 'NONE', #34066, #88975, #14162, .T. ) ;
#83129=CARTESIAN_POINT ( 'NONE',  ( 17.50000000000000711, 2.500000000000000444, 25.00000000000000000 ) ) ;
#83220=DIRECTION ( 'NONE',  ( 1.000000000000000000, 0.000000000000000000, 0.000000000000000000 ) ) ;
#83274=VERTEX_POINT ( 'NONE', #106668 ) ;
#83335=DIRECTION ( 'NONE',  ( 0.000000000000000000, -1.000000000000000000, -0.000000000000000000 ) ) ;
#83384=DIRECTION ( 'NONE',  ( 0.000000000000000000, 0.000000000000000000, -1.000000000000000000 ) ) ;
#83670=AXIS2_PLACEMENT_3D ( 'NONE', #48234, #65502, #6729 ) ;
#84279=LINE ( 'NONE', #26096, #20517 ) ;
#85025=VERTEX_POINT ( 'NONE', #88297 ) ;
#85037=CARTESIAN_POINT ( 'NONE',  ( 19.00000000000000711, 5.000000000000000888, 25.00000000000000000 ) ) ;
#85170=CARTESIAN_POINT ( 'NONE',  ( 20.00000000000000711, 5.000000000000000888, 25.00000000000000000 ) ) ;
#85276=LINE ( 'NONE', #68025, #86950 ) ;
#85364=ORIENTED_EDGE ( 'NONE', *, *, #11292, .T. ) ;
#85420=CARTESIAN_POINT ( 'NONE',  ( -19.99999999999999289, 5.000000000000000888, 25.00000000000000000 ) ) ;
#85721=EDGE_CURVE ( 'NONE', #88346, #34066, #85276, .T. ) ;
#85746=AXIS2_PLACEMENT_3D ( 'NONE', #67997, #34604, #1094 ) ;
#85896=CARTESIAN_POINT ( 'NONE',  ( -17.49999999999999645, 2.500000000000000444, 25.00000000000000000 ) ) ;
#86284=CIRCLE ( 'NONE', #22625, 1.000000000000000000 ) ;
#86331=CIRCLE ( 'NONE', #24280, 1.000000000000000888 ) ;
#86727=FACE_OUTER_BOUND ( 'NONE', #95764, .T. ) ;
#86909=( GEOMETRIC_REPRESENTATION_CONTEXT ( 3 ) GLOBAL_UNCERTAINTY_ASSIGNED_CONTEXT ( ( #76107 ) ) GLOBAL_UNIT_ASSIGNED_CONTEXT ( ( #79735, #79205, #77621 ) ) REPRESENTATION_CONTEXT ( 'NONE', 'WORKASPACE' ) );
#86950=VECTOR ( 'NONE', #3296, 1000.000000000000000 ) ;
#87288=EDGE_CURVE ( 'NONE', #50075, #88346, #94064, .T. ) ;
#87418=FACE_OUTER_BOUND ( 'NONE', #56284, .T. ) ;
#87556=FACE_OUTER_BOUND ( 'NONE', #102221, .T. ) ;
#88005=VERTEX_POINT ( 'NONE', #46879 ) ;
#88084=DIRECTION ( 'NONE',  ( 0.000000000000000000, 0.000000000000000000, -1.000000000000000000 ) ) ;
#88215=EDGE_LOOP ( 'NONE', ( #98093, #69529, #8231 ) ) ;
#88297=CARTESIAN_POINT ( 'NONE',  ( -17.49999999999999645, 2.500000000000000444, 25.00000000000000000 ) ) ;
#88346=VERTEX_POINT ( 'NONE', #49291 ) ;
#88367=EDGE_CURVE ( 'NONE', #6335, #34066, #61309, .T. ) ;
#88570=LINE ( 'NONE', #64304, #63172 ) ;
#88660=SPHERICAL_SURFACE ( 'NONE', #103095, 1.000000000000000000 ) ;
#88707=FACE_OUTER_BOUND ( 'NONE', #32137, .T. ) ;
#88749=ORIENTED_EDGE ( 'NONE', *, *, #91473, .T. ) ;
#88952=ORIENTED_EDGE ( 'NONE', *, *, #66910, .F. ) ;
#88975=VERTEX_POINT ( 'NONE', #54764 ) ;
#89033=CARTESIAN_POINT ( 'NONE',  ( -18.99999999999999289, -4.000000000000000000, -1.500000000000001332 ) ) ;
#89063=VECTOR ( 'NONE', #99131, 1000.000000000000000 ) ;
#89120=ORIENTED_EDGE ( 'NONE', *, *, #91473, .F. ) ;
#89192=FACE_BOUND ( 'NONE', #60729, .T. ) ;
#89273=DIRECTION ( 'NONE',  ( 1.000000000000000000, 0.000000000000000000, -0.000000000000000000 ) ) ;
#89412=ADVANCED_FACE ( 'NONE', ( #42576 ), #2103, .F. ) ;
#89423=VECTOR ( 'NONE', #62326, 1000.000000000000000 ) ;
#89645=VECTOR ( 'NONE', #6078, 1000.000000000000000 ) ;
#89866=DIRECTION ( 'NONE',  ( 0.000000000000000000, 0.000000000000000000, 1.000000000000000000 ) ) ;
#89957=APPLICATION_CONTEXT ( 'automotive_design' ) ;
#90014=CARTESIAN_POINT ( 'NONE',  ( -18.99999999999999289, -4.000000000000000000, -1.500000000000000000 ) ) ;
#90251=EDGE_CURVE ( 'NONE', #34066, #92851, #98437, .T. ) ;
#90364=( NAMED_UNIT ( * ) PLANE_ANGLE_UNIT ( ) SI_UNIT ( $, .RADIAN. ) );
#90512=VECTOR ( 'NONE', #44899, 1000.000000000000000 ) ;
#90678=CYLINDRICAL_SURFACE ( 'NONE', #85746, 1.000000000000000888 ) ;
#90764=ORIENTED_EDGE ( 'NONE', *, *, #74259, .F. ) ;
#90777=LINE ( 'NONE', #68086, #94783 ) ;
#90937=CARTESIAN_POINT ( 'NONE',  ( 19.00000000000001066, -4.000000000000000000, -1.500000000000001332 ) ) ;
#91243=AXIS2_PLACEMENT_3D ( 'NONE', #85170, #59852, #1014 ) ;
#91311=CARTESIAN_POINT ( 'NONE',  ( 19.00000000000001066, -4.000000000000000000, -1.500000000000001332 ) ) ;
#91343=AXIS2_PLACEMENT_3D ( 'NONE', #90937, #49925, #808 ) ;
#91473=EDGE_CURVE ( 'NONE', #72947, #6171, #90777, .T. ) ;
#91499=CARTESIAN_POINT ( 'NONE',  ( 19.00000000000001421, -3.999999999999999112, -1.500000000000000000 ) ) ;
#92318=AXIS2_PLACEMENT_3D ( 'NONE', #60914, #36138, #77078 ) ;
#92497=ADVANCED_FACE ( 'NONE', ( #88707 ), #104897, .T. ) ;
#92851=VERTEX_POINT ( 'NONE', #6576 ) ;
#93092=PRODUCT_DEFINITION_CONTEXT ( 'detailed design', #52789, 'design' ) ;
#93207=ORIENTED_EDGE ( 'NONE', *, *, #11170, .T. ) ;
#93351=EDGE_CURVE ( 'NONE', #81772, #7556, #106740, .T. ) ;
#93468=DIRECTION ( 'NONE',  ( 0.000000000000000000, 0.000000000000000000, -1.000000000000000000 ) ) ;
#93587=ORIENTED_EDGE ( 'NONE', *, *, #29244, .T. ) ;
#93743=( GEOMETRIC_REPRESENTATION_CONTEXT ( 3 ) GLOBAL_UNCERTAINTY_ASSIGNED_CONTEXT ( ( #40283 ) ) GLOBAL_UNIT_ASSIGNED_CONTEXT ( ( #53360, #36156, #37747 ) ) REPRESENTATION_CONTEXT ( 'NONE', 'WORKASPACE' ) );
#93822=SURFACE_STYLE_FILL_AREA ( #4810 ) ;
#93971=LINE ( 'NONE', #85896, #90512 ) ;
#94008=AXIS2_PLACEMENT_3D ( 'NONE', #8682, #7604, #98737 ) ;
#94064=LINE ( 'NONE', #10474, #102402 ) ;
#94413=AXIS2_PLACEMENT_3D ( 'NONE', #19346, #58693, #75388 ) ;
#94614=CLOSED_SHELL ( 'NONE', ( #43456, #35760, #30500, #89412, #56842, #44745, #92497, #47980, #28237, #35548, #3016, #102332, #21921, #80589, #13356, #33339, #35984, #39510, #80222, #7796, #44377, #80143, #63507 ) ) ;
#94737=FACE_OUTER_BOUND ( 'NONE', #49042, .T. ) ;
#94783=VECTOR ( 'NONE', #66485, 1000.000000000000000 ) ;
#94866=DIRECTION ( 'NONE',  ( -0.000000000000000000, -0.000000000000000000, -1.000000000000000000 ) ) ;
#95328=ORIENTED_EDGE ( 'NONE', *, *, #42972, .F. ) ;
#95451=LINE ( 'NONE', #53919, #65626 ) ;
#95764=EDGE_LOOP ( 'NONE', ( #53264, #10183, #57416, #72144 ) ) ;
#95774=CARTESIAN_POINT ( 'NONE',  ( 19.00000000000000711, 4.000000000000000000, -2.500000000000000000 ) ) ;
#96115=DIRECTION ( 'NONE',  ( 1.000000000000000000, 0.000000000000000000, -0.000000000000000000 ) ) ;
#96506=DIRECTION ( 'NONE',  ( -0.000000000000000000, -0.000000000000000000, -1.000000000000000000 ) ) ;
#96622=CARTESIAN_POINT ( 'NONE',  ( 20.00000000000000711, 4.000000000000000888, 25.00000000000000000 ) ) ;
#96639=ORIENTED_EDGE ( 'NONE', *, *, #31787, .T. ) ;
#96983=CARTESIAN_POINT ( 'NONE',  ( -18.99999999999999289, -4.000000000000000000, -1.500000000000001332 ) ) ;
#97156=FACE_OUTER_BOUND ( 'NONE', #59387, .T. ) ;
#97174=DIRECTION ( 'NONE',  ( 1.000000000000000000, 0.000000000000000000, 0.000000000000000000 ) ) ;
#97194=COLOUR_RGB ( '', 0.31764706, 0.68627451, 0.89019608) ;
#97527=CARTESIAN_POINT ( 'NONE',  ( -17.49999999999999645, 2.500000000000000444, 25.00000000000000000 ) ) ;
#97538=ORIENTED_EDGE ( 'NONE', *, *, #88367, .T. ) ;
#98093=ORIENTED_EDGE ( 'NONE', *, *, #81625, .T. ) ;
#98174=DIRECTION ( 'NONE',  ( 0.000000000000000000, 1.000000000000000000, 0.000000000000000000 ) ) ;
#98290=CARTESIAN_POINT ( 'NONE',  ( -18.99999999999999289, -5.000000000000000000, 25.00000000000000000 ) ) ;
#98437=LINE ( 'NONE', #22471, #70513 ) ;
#98727=FACE_OUTER_BOUND ( 'NONE', #18418, .T. ) ;
#98737=DIRECTION ( 'NONE',  ( -1.000000000000000000, 0.000000000000000000, 0.000000000000000000 ) ) ;
#98855=CARTESIAN_POINT ( 'NONE',  ( 19.00000000000000711, 4.000000000000000888, 25.00000000000000000 ) ) ;
#98998=LINE ( 'NONE', #57478, #51620 ) ;
#99131=DIRECTION ( 'NONE',  ( -0.000000000000000000, -0.000000000000000000, 1.000000000000000000 ) ) ;
#99759=SURFACE_STYLE_FILL_AREA ( #66873 ) ;
#99897=ORIENTED_EDGE ( 'NONE', *, *, #53580, .F. ) ;
#99901=LINE ( 'NONE', #42196, #105415 ) ;
#100280=ORIENTED_EDGE ( 'NONE', *, *, #58352, .T. ) ;
#100344=ORIENTED_EDGE ( 'NONE', *, *, #74259, .T. ) ;
#100345=ORIENTED_EDGE ( 'NONE', *, *, #26991, .T. ) ;
#100804=DIRECTION ( 'NONE',  ( -1.000000000000000000, 0.000000000000000000, 0.000000000000000000 ) ) ;
#101206=CIRCLE ( 'NONE', #78778, 1.000000000000000888 ) ;
#101352=DIRECTION ( 'NONE',  ( -3.469446951953614189E-16, 1.000000000000000000, 0.000000000000000000 ) ) ;
#101374=ORIENTED_EDGE ( 'NONE', *, *, #26991, .F. ) ;
#101477=CARTESIAN_POINT ( 'NONE',  ( -18.99999999999999645, -4.000000000000000000, -1.500000000000000000 ) ) ;
#101655=ORIENTED_EDGE ( 'NONE', *, *, #40700, .F. ) ;
#101889=EDGE_CURVE ( 'NONE', #7556, #88346, #101206, .T. ) ;
#101948=DIRECTION ( 'NONE',  ( -0.000000000000000000, 1.000000000000000000, 0.000000000000000000 ) ) ;
#102221=EDGE_LOOP ( 'NONE', ( #36929, #43706, #1606, #79285 ) ) ;
#102332=ADVANCED_FACE ( 'NONE', ( #59389 ), #90678, .T. ) ;
#102402=VECTOR ( 'NONE', #60658, 1000.000000000000000 ) ;
#102411=CARTESIAN_POINT ( 'NONE',  ( 20.00000000000001066, -4.000000000000000000, 25.00000000000000000 ) ) ;
#102651=CIRCLE ( 'NONE', #92318, 1.000000000000000888 ) ;
#102888=VECTOR ( 'NONE', #40540, 1000.000000000000000 ) ;
#102914=ORIENTED_EDGE ( 'NONE', *, *, #66910, .T. ) ;
#102975=PRESENTATION_STYLE_ASSIGNMENT (( #70075 ) ) ;
#103095=AXIS2_PLACEMENT_3D ( 'NONE', #89033, #98174, #24328 ) ;
#103185=ORIENTED_EDGE ( 'NONE', *, *, #87288, .F. ) ;
#103757=ORIENTED_EDGE ( 'NONE', *, *, #49584, .T. ) ;
#103856=PLANE ( 'NONE',  #38018 ) ;
#104041=STYLED_ITEM ( 'NONE', ( #102975 ), #64127 ) ;
#104796=DIRECTION ( 'NONE',  ( 0.000000000000000000, 0.000000000000000000, -1.000000000000000000 ) ) ;
#104897=PLANE ( 'NONE',  #57014 ) ;
#104924=VERTEX_POINT ( 'NONE', #43826 ) ;
#105013=ORIENTED_EDGE ( 'NONE', *, *, #19065, .F. ) ;
#105263=PLANE ( 'NONE',  #7834 ) ;
#105415=VECTOR ( 'NONE', #75079, 1000.000000000000000 ) ;
#105545=DIRECTION ( 'NONE',  ( -1.000000000000000000, -2.168404344971008868E-17, 0.000000000000000000 ) ) ;
#105609=DIRECTION ( 'NONE',  ( -0.000000000000000000, -0.000000000000000000, 1.000000000000000000 ) ) ;
#105639=LINE ( 'NONE', #65190, #89063 ) ;
#105657=EDGE_LOOP ( 'NONE', ( #41054, #100345, #55490 ) ) ;
#105664=DIRECTION ( 'NONE',  ( -1.000000000000000000, -0.000000000000000000, -0.000000000000000000 ) ) ;
#105725=ORIENTED_EDGE ( 'NONE', *, *, #7201, .T. ) ;
#106088=ORIENTED_EDGE ( 'NONE', *, *, #19066, .F. ) ;
#106175=DIRECTION ( 'NONE',  ( -0.000000000000000000, -1.000000000000000000, 0.000000000000000000 ) ) ;
#106251=ORIENTED_EDGE ( 'NONE', *, *, #47123, .F. ) ;
#106409=DIRECTION ( 'NONE',  ( -0.000000000000000000, 0.000000000000000000, 1.000000000000000000 ) ) ;
#106659=VECTOR ( 'NONE', #58463, 1000.000000000000000 ) ;
#106668=CARTESIAN_POINT ( 'NONE',  ( -17.49999999999999645, 2.500000000000000444, 0.000000000000000000 ) ) ;
#106740=LINE ( 'NONE', #23204, #70967 ) ;
#106755=EDGE_CURVE ( 'NONE', #74216, #68599, #38710, .T. ) ;
ENDSEC;
END-ISO-10303-21;
